ISO-10303-21;
HEADER;
/* Generated by software containing ST-Developer
 * from STEP Tools, Inc. (www.steptools.com) 
 */

FILE_DESCRIPTION(
/* description */ (''),
/* implementation_level */ '2;1');

FILE_NAME(
/* name */ 'Clamp_01.step',
/* time_stamp */ '2026-10-22T13:39:42+06:00',
/* author */ (''),
/* organization */ (''),
/* preprocessor_version */ 'ST-DEVELOPER v20.2',
/* originating_system */ 'Autodesk Translation Framework v15.15.0.0',
/* authorisation */ '');

FILE_SCHEMA (('AUTOMOTIVE_DESIGN { 1 0 10303 214 3 1 1 }'));
ENDSEC;

DATA;
#10=MECHANICAL_DESIGN_GEOMETRIC_PRESENTATION_REPRESENTATION('',(#313),#17836);
#187=SPHERICAL_SURFACE('',#10736,0.299999999999994);
#188=SPHERICAL_SURFACE('',#10747,0.3);
#189=SPHERICAL_SURFACE('',#10751,0.299999999999994);
#190=SPHERICAL_SURFACE('',#10756,0.3);
#191=SPHERICAL_SURFACE('',#10760,0.300000000000011);
#192=SPHERICAL_SURFACE('',#10764,0.300000000000003);
#193=SPHERICAL_SURFACE('',#10768,0.299999999999994);
#194=SPHERICAL_SURFACE('',#10773,0.300000000000011);
#249=TOROIDAL_SURFACE('',#10718,4.79999999999999,0.3);
#250=TOROIDAL_SURFACE('',#10724,4.79999999999998,0.3);
#251=TOROIDAL_SURFACE('',#10731,0.600000000000001,0.3);
#252=TOROIDAL_SURFACE('',#10740,0.600000000000001,0.300000000000011);
#253=TOROIDAL_SURFACE('',#10803,4.79999999999998,0.3);
#254=TOROIDAL_SURFACE('',#10808,4.79999999999999,0.3);
#281=ELLIPSE('',#10746,0.424264068711946,0.3);
#282=ELLIPSE('',#10790,0.424264068711924,0.3);
#293=SHAPE_REPRESENTATION_RELATIONSHIP('SRR','None',#17880,#303);
#303=ADVANCED_BREP_SHAPE_REPRESENTATION('',(#323),#17832);
#313=STYLED_ITEM('',(#17959),#323);
#323=MANIFOLD_SOLID_BREP('Clamp_01',#9634);
#569=CYLINDRICAL_SURFACE('',#10715,0.3);
#570=CYLINDRICAL_SURFACE('',#10722,0.3);
#571=CYLINDRICAL_SURFACE('',#10727,4.49999999999999);
#572=CYLINDRICAL_SURFACE('',#10745,0.3);
#573=CYLINDRICAL_SURFACE('',#10755,0.3);
#574=CYLINDRICAL_SURFACE('',#10772,0.3);
#575=CYLINDRICAL_SURFACE('',#10777,0.3);
#576=CYLINDRICAL_SURFACE('',#10778,0.3);
#577=CYLINDRICAL_SURFACE('',#10779,0.3);
#578=CYLINDRICAL_SURFACE('',#10780,0.3);
#579=CYLINDRICAL_SURFACE('',#10781,0.3);
#580=CYLINDRICAL_SURFACE('',#10782,0.3);
#581=CYLINDRICAL_SURFACE('',#10783,0.3);
#582=CYLINDRICAL_SURFACE('',#10784,0.3);
#583=CYLINDRICAL_SURFACE('',#10785,0.3);
#584=CYLINDRICAL_SURFACE('',#10786,0.3);
#585=CYLINDRICAL_SURFACE('',#10787,0.3);
#586=CYLINDRICAL_SURFACE('',#10788,0.3);
#587=CYLINDRICAL_SURFACE('',#10789,0.3);
#588=CYLINDRICAL_SURFACE('',#10791,0.3);
#589=CYLINDRICAL_SURFACE('',#10800,0.3);
#590=CYLINDRICAL_SURFACE('',#10806,0.3);
#591=CYLINDRICAL_SURFACE('',#10809,4.49999999999998);
#1160=LINE('',#17194,#1825);
#1161=LINE('',#17197,#1826);
#1162=LINE('',#17208,#1827);
#1163=LINE('',#17209,#1828);
#1164=LINE('',#17215,#1829);
#1165=LINE('',#17218,#1830);
#1166=LINE('',#17221,#1831);
#1167=LINE('',#17222,#1832);
#1168=LINE('',#17226,#1833);
#1169=LINE('',#17228,#1834);
#1170=LINE('',#17230,#1835);
#1171=LINE('',#17231,#1836);
#1172=LINE('',#17257,#1837);
#1173=LINE('',#17259,#1838);
#1174=LINE('',#17275,#1839);
#1175=LINE('',#17276,#1840);
#1176=LINE('',#17305,#1841);
#1177=LINE('',#17306,#1842);
#1178=LINE('',#17315,#1843);
#1179=LINE('',#17316,#1844);
#1180=LINE('',#17318,#1845);
#1181=LINE('',#17319,#1846);
#1182=LINE('',#17321,#1847);
#1183=LINE('',#17322,#1848);
#1184=LINE('',#17324,#1849);
#1185=LINE('',#17325,#1850);
#1186=LINE('',#17327,#1851);
#1187=LINE('',#17328,#1852);
#1188=LINE('',#17330,#1853);
#1189=LINE('',#17331,#1854);
#1190=LINE('',#17333,#1855);
#1191=LINE('',#17335,#1856);
#1192=LINE('',#17337,#1857);
#1193=LINE('',#17338,#1858);
#1194=LINE('',#17340,#1859);
#1195=LINE('',#17341,#1860);
#1196=LINE('',#17343,#1861);
#1197=LINE('',#17345,#1862);
#1198=LINE('',#17348,#1863);
#1199=LINE('',#17350,#1864);
#1200=LINE('',#17353,#1865);
#1201=LINE('',#17354,#1866);
#1202=LINE('',#17356,#1867);
#1203=LINE('',#17362,#1868);
#1204=LINE('',#17366,#1869);
#1205=LINE('',#17379,#1870);
#1206=LINE('',#17382,#1871);
#1825=VECTOR('',#13488,10.);
#1826=VECTOR('',#13491,10.);
#1827=VECTOR('',#13504,10.);
#1828=VECTOR('',#13505,10.);
#1829=VECTOR('',#13514,10.);
#1830=VECTOR('',#13517,10.);
#1831=VECTOR('',#13520,10.);
#1832=VECTOR('',#13521,10.);
#1833=VECTOR('',#13524,10.);
#1834=VECTOR('',#13525,10.);
#1835=VECTOR('',#13526,10.);
#1836=VECTOR('',#13527,10.);
#1837=VECTOR('',#13558,10.);
#1838=VECTOR('',#13559,10.);
#1839=VECTOR('',#13580,10.);
#1840=VECTOR('',#13581,10.);
#1841=VECTOR('',#13616,10.);
#1842=VECTOR('',#13617,10.);
#1843=VECTOR('',#13628,10.);
#1844=VECTOR('',#13629,10.);
#1845=VECTOR('',#13632,10.);
#1846=VECTOR('',#13633,10.);
#1847=VECTOR('',#13636,10.);
#1848=VECTOR('',#13637,10.);
#1849=VECTOR('',#13640,10.);
#1850=VECTOR('',#13641,10.);
#1851=VECTOR('',#13644,10.);
#1852=VECTOR('',#13645,10.);
#1853=VECTOR('',#13648,10.);
#1854=VECTOR('',#13649,10.);
#1855=VECTOR('',#13652,10.);
#1856=VECTOR('',#13655,10.);
#1857=VECTOR('',#13658,10.);
#1858=VECTOR('',#13659,10.);
#1859=VECTOR('',#13662,10.);
#1860=VECTOR('',#13663,10.);
#1861=VECTOR('',#13666,10.);
#1862=VECTOR('',#13669,10.);
#1863=VECTOR('',#13672,10.);
#1864=VECTOR('',#13673,10.);
#1865=VECTOR('',#13678,10.);
#1866=VECTOR('',#13679,10.);
#1867=VECTOR('',#13682,10.);
#1868=VECTOR('',#13689,10.);
#1869=VECTOR('',#13692,10.);
#1870=VECTOR('',#13715,10.);
#1871=VECTOR('',#13720,10.);
#2020=FACE_BOUND('',#3160,.T.);
#2021=FACE_BOUND('',#3192,.T.);
#2493=FACE_OUTER_BOUND('',#3153,.T.);
#2494=FACE_OUTER_BOUND('',#3154,.T.);
#2495=FACE_OUTER_BOUND('',#3155,.T.);
#2496=FACE_OUTER_BOUND('',#3156,.T.);
#2497=FACE_OUTER_BOUND('',#3157,.T.);
#2498=FACE_OUTER_BOUND('',#3158,.T.);
#2499=FACE_OUTER_BOUND('',#3159,.T.);
#2500=FACE_OUTER_BOUND('',#3161,.T.);
#2501=FACE_OUTER_BOUND('',#3162,.T.);
#2502=FACE_OUTER_BOUND('',#3163,.T.);
#2503=FACE_OUTER_BOUND('',#3164,.T.);
#2504=FACE_OUTER_BOUND('',#3165,.T.);
#2505=FACE_OUTER_BOUND('',#3166,.T.);
#2506=FACE_OUTER_BOUND('',#3167,.T.);
#2507=FACE_OUTER_BOUND('',#3168,.T.);
#2508=FACE_OUTER_BOUND('',#3169,.T.);
#2509=FACE_OUTER_BOUND('',#3170,.T.);
#2510=FACE_OUTER_BOUND('',#3171,.T.);
#2511=FACE_OUTER_BOUND('',#3172,.T.);
#2512=FACE_OUTER_BOUND('',#3173,.T.);
#2513=FACE_OUTER_BOUND('',#3174,.T.);
#2514=FACE_OUTER_BOUND('',#3175,.T.);
#2515=FACE_OUTER_BOUND('',#3176,.T.);
#2516=FACE_OUTER_BOUND('',#3177,.T.);
#2517=FACE_OUTER_BOUND('',#3178,.T.);
#2518=FACE_OUTER_BOUND('',#3179,.T.);
#2519=FACE_OUTER_BOUND('',#3180,.T.);
#2520=FACE_OUTER_BOUND('',#3181,.T.);
#2521=FACE_OUTER_BOUND('',#3182,.T.);
#2522=FACE_OUTER_BOUND('',#3183,.T.);
#2523=FACE_OUTER_BOUND('',#3184,.T.);
#2524=FACE_OUTER_BOUND('',#3185,.T.);
#2525=FACE_OUTER_BOUND('',#3186,.T.);
#2526=FACE_OUTER_BOUND('',#3187,.T.);
#2527=FACE_OUTER_BOUND('',#3188,.T.);
#2528=FACE_OUTER_BOUND('',#3189,.T.);
#2529=FACE_OUTER_BOUND('',#3190,.T.);
#2530=FACE_OUTER_BOUND('',#3191,.T.);
#2531=FACE_OUTER_BOUND('',#3193,.T.);
#2532=FACE_OUTER_BOUND('',#3194,.T.);
#2533=FACE_OUTER_BOUND('',#3195,.T.);
#2534=FACE_OUTER_BOUND('',#3196,.T.);
#2535=FACE_OUTER_BOUND('',#3197,.T.);
#2536=FACE_OUTER_BOUND('',#3198,.T.);
#2537=FACE_OUTER_BOUND('',#3199,.T.);
#2538=FACE_OUTER_BOUND('',#3200,.T.);
#2539=FACE_OUTER_BOUND('',#3201,.T.);
#3153=EDGE_LOOP('',(#8263,#8264,#8265,#8266));
#3154=EDGE_LOOP('',(#8267,#8268,#8269,#8270));
#3155=EDGE_LOOP('',(#8271,#8272,#8273,#8274));
#3156=EDGE_LOOP('',(#8275,#8276,#8277,#8278));
#3157=EDGE_LOOP('',(#8279,#8280,#8281,#8282));
#3158=EDGE_LOOP('',(#8283,#8284,#8285,#8286));
#3159=EDGE_LOOP('',(#8287,#8288,#8289,#8290));
#3160=EDGE_LOOP('',(#8291,#8292,#8293,#8294));
#3161=EDGE_LOOP('',(#8295,#8296,#8297,#8298));
#3162=EDGE_LOOP('',(#8299,#8300,#8301));
#3163=EDGE_LOOP('',(#8302,#8303,#8304,#8305));
#3164=EDGE_LOOP('',(#8306,#8307,#8308,#8309));
#3165=EDGE_LOOP('',(#8310,#8311,#8312));
#3166=EDGE_LOOP('',(#8313,#8314,#8315));
#3167=EDGE_LOOP('',(#8316,#8317,#8318,#8319));
#3168=EDGE_LOOP('',(#8320,#8321,#8322));
#3169=EDGE_LOOP('',(#8323,#8324,#8325));
#3170=EDGE_LOOP('',(#8326,#8327,#8328));
#3171=EDGE_LOOP('',(#8329,#8330,#8331));
#3172=EDGE_LOOP('',(#8332,#8333,#8334,#8335));
#3173=EDGE_LOOP('',(#8336,#8337,#8338));
#3174=EDGE_LOOP('',(#8339,#8340,#8341,#8342));
#3175=EDGE_LOOP('',(#8343,#8344,#8345,#8346));
#3176=EDGE_LOOP('',(#8347,#8348,#8349,#8350));
#3177=EDGE_LOOP('',(#8351,#8352,#8353,#8354));
#3178=EDGE_LOOP('',(#8355,#8356,#8357,#8358));
#3179=EDGE_LOOP('',(#8359,#8360,#8361,#8362));
#3180=EDGE_LOOP('',(#8363,#8364,#8365,#8366));
#3181=EDGE_LOOP('',(#8367,#8368,#8369,#8370));
#3182=EDGE_LOOP('',(#8371,#8372,#8373,#8374));
#3183=EDGE_LOOP('',(#8375,#8376,#8377,#8378));
#3184=EDGE_LOOP('',(#8379,#8380,#8381,#8382));
#3185=EDGE_LOOP('',(#8383,#8384,#8385,#8386));
#3186=EDGE_LOOP('',(#8387,#8388,#8389,#8390));
#3187=EDGE_LOOP('',(#8391,#8392,#8393,#8394));
#3188=EDGE_LOOP('',(#8395,#8396,#8397,#8398));
#3189=EDGE_LOOP('',(#8399,#8400,#8401,#8402,#8403,#8404,#8405));
#3190=EDGE_LOOP('',(#8406,#8407,#8408,#8409));
#3191=EDGE_LOOP('',(#8410,#8411,#8412,#8413));
#3192=EDGE_LOOP('',(#8414,#8415,#8416,#8417));
#3193=EDGE_LOOP('',(#8418,#8419,#8420,#8421));
#3194=EDGE_LOOP('',(#8422,#8423,#8424,#8425,#8426,#8427,#8428));
#3195=EDGE_LOOP('',(#8429,#8430,#8431,#8432));
#3196=EDGE_LOOP('',(#8433,#8434,#8435,#8436));
#3197=EDGE_LOOP('',(#8437,#8438,#8439,#8440));
#3198=EDGE_LOOP('',(#8441,#8442,#8443,#8444));
#3199=EDGE_LOOP('',(#8445,#8446,#8447,#8448));
#3200=EDGE_LOOP('',(#8449,#8450,#8451,#8452));
#3201=EDGE_LOOP('',(#8453,#8454,#8455,#8456));
#3786=CIRCLE('',#10716,0.3);
#3787=CIRCLE('',#10717,0.299999999999994);
#3788=CIRCLE('',#10719,0.300000000000011);
#3789=CIRCLE('',#10720,4.79999999999999);
#3790=CIRCLE('',#10721,4.49999999999999);
#3791=CIRCLE('',#10723,0.300000000000002);
#3792=CIRCLE('',#10725,4.79999999999998);
#3793=CIRCLE('',#10726,4.49999999999998);
#3794=CIRCLE('',#10728,4.49999999999999);
#3795=CIRCLE('',#10732,0.3);
#3796=CIRCLE('',#10733,0.299999999999994);
#3797=CIRCLE('',#10734,0.300000000000011);
#3798=CIRCLE('',#10735,0.599999999999987);
#3799=CIRCLE('',#10737,0.3);
#3800=CIRCLE('',#10738,0.299999999999994);
#3801=CIRCLE('',#10739,0.300000000000011);
#3802=CIRCLE('',#10741,0.600000000000001);
#3803=CIRCLE('',#10742,0.299999999999976);
#3804=CIRCLE('',#10743,0.3);
#3805=CIRCLE('',#10744,0.300000000000011);
#3806=CIRCLE('',#10748,0.300000000000003);
#3807=CIRCLE('',#10749,0.3);
#3808=CIRCLE('',#10750,0.300000000000011);
#3809=CIRCLE('',#10752,0.3);
#3810=CIRCLE('',#10753,0.299999999999994);
#3811=CIRCLE('',#10754,0.300000000000011);
#3812=CIRCLE('',#10757,0.299999999999994);
#3813=CIRCLE('',#10758,0.3);
#3814=CIRCLE('',#10759,0.300000000000011);
#3815=CIRCLE('',#10761,0.300000000000006);
#3816=CIRCLE('',#10762,0.300000000000011);
#3817=CIRCLE('',#10763,0.3);
#3818=CIRCLE('',#10765,0.3);
#3819=CIRCLE('',#10766,0.300000000000003);
#3820=CIRCLE('',#10767,0.300000000000011);
#3821=CIRCLE('',#10769,0.300000000000011);
#3822=CIRCLE('',#10770,0.299999999999994);
#3823=CIRCLE('',#10771,0.3);
#3824=CIRCLE('',#10774,0.3);
#3825=CIRCLE('',#10775,0.300000000000011);
#3826=CIRCLE('',#10776,0.300000000000001);
#3827=CIRCLE('',#10796,4.79999999999998);
#3828=CIRCLE('',#10797,4.79999999999999);
#3829=CIRCLE('',#10801,0.3);
#3830=CIRCLE('',#10802,0.299999999999994);
#3831=CIRCLE('',#10804,0.300000000000002);
#3832=CIRCLE('',#10805,4.49999999999998);
#3833=CIRCLE('',#10807,0.300000000000002);
#4560=VERTEX_POINT('',#17190);
#4561=VERTEX_POINT('',#17191);
#4562=VERTEX_POINT('',#17193);
#4563=VERTEX_POINT('',#17195);
#4564=VERTEX_POINT('',#17199);
#4565=VERTEX_POINT('',#17200);
#4566=VERTEX_POINT('',#17205);
#4567=VERTEX_POINT('',#17206);
#4568=VERTEX_POINT('',#17214);
#4569=VERTEX_POINT('',#17216);
#4570=VERTEX_POINT('',#17220);
#4571=VERTEX_POINT('',#17224);
#4572=VERTEX_POINT('',#17225);
#4573=VERTEX_POINT('',#17227);
#4574=VERTEX_POINT('',#17229);
#4575=VERTEX_POINT('',#17233);
#4576=VERTEX_POINT('',#17235);
#4577=VERTEX_POINT('',#17237);
#4578=VERTEX_POINT('',#17241);
#4579=VERTEX_POINT('',#17242);
#4580=VERTEX_POINT('',#17244);
#4581=VERTEX_POINT('',#17248);
#4582=VERTEX_POINT('',#17249);
#4583=VERTEX_POINT('',#17251);
#4584=VERTEX_POINT('',#17256);
#4585=VERTEX_POINT('',#17258);
#4586=VERTEX_POINT('',#17262);
#4587=VERTEX_POINT('',#17263);
#4588=VERTEX_POINT('',#17268);
#4589=VERTEX_POINT('',#17269);
#4590=VERTEX_POINT('',#17271);
#4591=VERTEX_POINT('',#17278);
#4592=VERTEX_POINT('',#17279);
#4593=VERTEX_POINT('',#17281);
#4594=VERTEX_POINT('',#17285);
#4595=VERTEX_POINT('',#17287);
#4596=VERTEX_POINT('',#17291);
#4597=VERTEX_POINT('',#17292);
#4598=VERTEX_POINT('',#17294);
#4599=VERTEX_POINT('',#17298);
#4600=VERTEX_POINT('',#17299);
#4601=VERTEX_POINT('',#17301);
#4602=VERTEX_POINT('',#17308);
#4603=VERTEX_POINT('',#17309);
#4604=VERTEX_POINT('',#17311);
#4605=VERTEX_POINT('',#17347);
#4606=VERTEX_POINT('',#17349);
#4607=VERTEX_POINT('',#17360);
#4608=VERTEX_POINT('',#17361);
#4609=VERTEX_POINT('',#17363);
#4610=VERTEX_POINT('',#17365);
#4611=VERTEX_POINT('',#17374);
#5802=EDGE_CURVE('',#4560,#4561,#3786,.T.);
#5803=EDGE_CURVE('',#4561,#4562,#1160,.T.);
#5804=EDGE_CURVE('',#4562,#4563,#3787,.T.);
#5805=EDGE_CURVE('',#4563,#4560,#1161,.T.);
#5806=EDGE_CURVE('',#4564,#4565,#3788,.T.);
#5807=EDGE_CURVE('',#4565,#4563,#3789,.T.);
#5808=EDGE_CURVE('',#4562,#4564,#3790,.T.);
#5809=EDGE_CURVE('',#4566,#4567,#3791,.T.);
#5810=EDGE_CURVE('',#4567,#4565,#1162,.T.);
#5811=EDGE_CURVE('',#4564,#4566,#1163,.T.);
#5812=EDGE_CURVE('',#4560,#4567,#3792,.T.);
#5813=EDGE_CURVE('',#4566,#4561,#3793,.T.);
#5814=EDGE_CURVE('',#4568,#4562,#1164,.T.);
#5815=EDGE_CURVE('',#4569,#4568,#3794,.T.);
#5816=EDGE_CURVE('',#4569,#4564,#1165,.T.);
#5817=EDGE_CURVE('',#4570,#4561,#1166,.T.);
#5818=EDGE_CURVE('',#4568,#4570,#1167,.T.);
#5819=EDGE_CURVE('',#4571,#4572,#1168,.T.);
#5820=EDGE_CURVE('',#4573,#4571,#1169,.T.);
#5821=EDGE_CURVE('',#4574,#4573,#1170,.T.);
#5822=EDGE_CURVE('',#4572,#4574,#1171,.T.);
#5823=EDGE_CURVE('',#4573,#4575,#3795,.T.);
#5824=EDGE_CURVE('',#4576,#4573,#3796,.F.);
#5825=EDGE_CURVE('',#4577,#4576,#3797,.T.);
#5826=EDGE_CURVE('',#4577,#4575,#3798,.T.);
#5827=EDGE_CURVE('',#4578,#4579,#3799,.F.);
#5828=EDGE_CURVE('',#4580,#4578,#3800,.F.);
#5829=EDGE_CURVE('',#4579,#4580,#3801,.F.);
#5830=EDGE_CURVE('',#4581,#4582,#3802,.T.);
#5831=EDGE_CURVE('',#4583,#4582,#3803,.T.);
#5832=EDGE_CURVE('',#4571,#4583,#3804,.F.);
#5833=EDGE_CURVE('',#4581,#4571,#3805,.T.);
#5834=EDGE_CURVE('',#4584,#4583,#1172,.T.);
#5835=EDGE_CURVE('',#4582,#4585,#1173,.T.);
#5836=EDGE_CURVE('',#4585,#4584,#281,.T.);
#5837=EDGE_CURVE('',#4586,#4587,#3806,.F.);
#5838=EDGE_CURVE('',#4574,#4586,#3807,.F.);
#5839=EDGE_CURVE('',#4587,#4574,#3808,.F.);
#5840=EDGE_CURVE('',#4588,#4589,#3809,.F.);
#5841=EDGE_CURVE('',#4590,#4588,#3810,.F.);
#5842=EDGE_CURVE('',#4589,#4590,#3811,.F.);
#5843=EDGE_CURVE('',#4585,#4590,#1174,.T.);
#5844=EDGE_CURVE('',#4588,#4584,#1175,.T.);
#5845=EDGE_CURVE('',#4591,#4592,#3812,.F.);
#5846=EDGE_CURVE('',#4593,#4591,#3813,.F.);
#5847=EDGE_CURVE('',#4592,#4593,#3814,.F.);
#5848=EDGE_CURVE('',#4594,#4572,#3815,.F.);
#5849=EDGE_CURVE('',#4595,#4594,#3816,.F.);
#5850=EDGE_CURVE('',#4572,#4595,#3817,.F.);
#5851=EDGE_CURVE('',#4596,#4597,#3818,.F.);
#5852=EDGE_CURVE('',#4598,#4596,#3819,.F.);
#5853=EDGE_CURVE('',#4597,#4598,#3820,.F.);
#5854=EDGE_CURVE('',#4599,#4600,#3821,.F.);
#5855=EDGE_CURVE('',#4601,#4599,#3822,.F.);
#5856=EDGE_CURVE('',#4600,#4601,#3823,.F.);
#5857=EDGE_CURVE('',#4599,#4589,#1176,.T.);
#5858=EDGE_CURVE('',#4590,#4601,#1177,.T.);
#5859=EDGE_CURVE('',#4602,#4603,#3824,.F.);
#5860=EDGE_CURVE('',#4604,#4602,#3825,.F.);
#5861=EDGE_CURVE('',#4603,#4604,#3826,.F.);
#5862=EDGE_CURVE('',#4601,#4604,#1178,.T.);
#5863=EDGE_CURVE('',#4602,#4600,#1179,.T.);
#5864=EDGE_CURVE('',#4604,#4595,#1180,.T.);
#5865=EDGE_CURVE('',#4594,#4603,#1181,.T.);
#5866=EDGE_CURVE('',#4596,#4602,#1182,.T.);
#5867=EDGE_CURVE('',#4603,#4598,#1183,.T.);
#5868=EDGE_CURVE('',#4591,#4599,#1184,.T.);
#5869=EDGE_CURVE('',#4600,#4593,#1185,.T.);
#5870=EDGE_CURVE('',#4587,#4597,#1186,.T.);
#5871=EDGE_CURVE('',#4598,#4586,#1187,.T.);
#5872=EDGE_CURVE('',#4597,#4592,#1188,.T.);
#5873=EDGE_CURVE('',#4593,#4596,#1189,.T.);
#5874=EDGE_CURVE('',#4595,#4581,#1190,.T.);
#5875=EDGE_CURVE('',#4586,#4594,#1191,.T.);
#5876=EDGE_CURVE('',#4592,#4579,#1192,.T.);
#5877=EDGE_CURVE('',#4580,#4591,#1193,.T.);
#5878=EDGE_CURVE('',#4578,#4588,#1194,.T.);
#5879=EDGE_CURVE('',#4589,#4580,#1195,.T.);
#5880=EDGE_CURVE('',#4575,#4587,#1196,.T.);
#5881=EDGE_CURVE('',#4583,#4576,#1197,.T.);
#5882=EDGE_CURVE('',#4605,#4578,#1198,.T.);
#5883=EDGE_CURVE('',#4579,#4606,#1199,.T.);
#5884=EDGE_CURVE('',#4606,#4605,#282,.T.);
#5885=EDGE_CURVE('',#4606,#4577,#1200,.T.);
#5886=EDGE_CURVE('',#4576,#4605,#1201,.T.);
#5887=EDGE_CURVE('',#4584,#4605,#1202,.T.);
#5888=EDGE_CURVE('',#4607,#4608,#1203,.T.);
#5889=EDGE_CURVE('',#4609,#4607,#3827,.T.);
#5890=EDGE_CURVE('',#4610,#4609,#1204,.T.);
#5891=EDGE_CURVE('',#4608,#4610,#3828,.T.);
#5892=EDGE_CURVE('',#4608,#4568,#3829,.T.);
#5893=EDGE_CURVE('',#4570,#4607,#3830,.T.);
#5894=EDGE_CURVE('',#4611,#4609,#3831,.T.);
#5895=EDGE_CURVE('',#4570,#4611,#3832,.T.);
#5896=EDGE_CURVE('',#4569,#4610,#3833,.T.);
#5897=EDGE_CURVE('',#4611,#4569,#1205,.T.);
#5898=EDGE_CURVE('',#4611,#4566,#1206,.T.);
#8263=ORIENTED_EDGE('',*,*,#5802,.T.);
#8264=ORIENTED_EDGE('',*,*,#5803,.T.);
#8265=ORIENTED_EDGE('',*,*,#5804,.T.);
#8266=ORIENTED_EDGE('',*,*,#5805,.T.);
#8267=ORIENTED_EDGE('',*,*,#5806,.T.);
#8268=ORIENTED_EDGE('',*,*,#5807,.T.);
#8269=ORIENTED_EDGE('',*,*,#5804,.F.);
#8270=ORIENTED_EDGE('',*,*,#5808,.T.);
#8271=ORIENTED_EDGE('',*,*,#5809,.T.);
#8272=ORIENTED_EDGE('',*,*,#5810,.T.);
#8273=ORIENTED_EDGE('',*,*,#5806,.F.);
#8274=ORIENTED_EDGE('',*,*,#5811,.T.);
#8275=ORIENTED_EDGE('',*,*,#5802,.F.);
#8276=ORIENTED_EDGE('',*,*,#5812,.T.);
#8277=ORIENTED_EDGE('',*,*,#5809,.F.);
#8278=ORIENTED_EDGE('',*,*,#5813,.T.);
#8279=ORIENTED_EDGE('',*,*,#5808,.F.);
#8280=ORIENTED_EDGE('',*,*,#5814,.F.);
#8281=ORIENTED_EDGE('',*,*,#5815,.F.);
#8282=ORIENTED_EDGE('',*,*,#5816,.T.);
#8283=ORIENTED_EDGE('',*,*,#5803,.F.);
#8284=ORIENTED_EDGE('',*,*,#5817,.F.);
#8285=ORIENTED_EDGE('',*,*,#5818,.F.);
#8286=ORIENTED_EDGE('',*,*,#5814,.T.);
#8287=ORIENTED_EDGE('',*,*,#5819,.F.);
#8288=ORIENTED_EDGE('',*,*,#5820,.F.);
#8289=ORIENTED_EDGE('',*,*,#5821,.F.);
#8290=ORIENTED_EDGE('',*,*,#5822,.F.);
#8291=ORIENTED_EDGE('',*,*,#5805,.F.);
#8292=ORIENTED_EDGE('',*,*,#5807,.F.);
#8293=ORIENTED_EDGE('',*,*,#5810,.F.);
#8294=ORIENTED_EDGE('',*,*,#5812,.F.);
#8295=ORIENTED_EDGE('',*,*,#5823,.F.);
#8296=ORIENTED_EDGE('',*,*,#5824,.F.);
#8297=ORIENTED_EDGE('',*,*,#5825,.F.);
#8298=ORIENTED_EDGE('',*,*,#5826,.T.);
#8299=ORIENTED_EDGE('',*,*,#5827,.F.);
#8300=ORIENTED_EDGE('',*,*,#5828,.F.);
#8301=ORIENTED_EDGE('',*,*,#5829,.F.);
#8302=ORIENTED_EDGE('',*,*,#5830,.T.);
#8303=ORIENTED_EDGE('',*,*,#5831,.F.);
#8304=ORIENTED_EDGE('',*,*,#5832,.F.);
#8305=ORIENTED_EDGE('',*,*,#5833,.F.);
#8306=ORIENTED_EDGE('',*,*,#5834,.T.);
#8307=ORIENTED_EDGE('',*,*,#5831,.T.);
#8308=ORIENTED_EDGE('',*,*,#5835,.T.);
#8309=ORIENTED_EDGE('',*,*,#5836,.T.);
#8310=ORIENTED_EDGE('',*,*,#5837,.F.);
#8311=ORIENTED_EDGE('',*,*,#5838,.F.);
#8312=ORIENTED_EDGE('',*,*,#5839,.F.);
#8313=ORIENTED_EDGE('',*,*,#5840,.F.);
#8314=ORIENTED_EDGE('',*,*,#5841,.F.);
#8315=ORIENTED_EDGE('',*,*,#5842,.F.);
#8316=ORIENTED_EDGE('',*,*,#5843,.T.);
#8317=ORIENTED_EDGE('',*,*,#5841,.T.);
#8318=ORIENTED_EDGE('',*,*,#5844,.T.);
#8319=ORIENTED_EDGE('',*,*,#5836,.F.);
#8320=ORIENTED_EDGE('',*,*,#5845,.F.);
#8321=ORIENTED_EDGE('',*,*,#5846,.F.);
#8322=ORIENTED_EDGE('',*,*,#5847,.F.);
#8323=ORIENTED_EDGE('',*,*,#5848,.F.);
#8324=ORIENTED_EDGE('',*,*,#5849,.F.);
#8325=ORIENTED_EDGE('',*,*,#5850,.F.);
#8326=ORIENTED_EDGE('',*,*,#5851,.F.);
#8327=ORIENTED_EDGE('',*,*,#5852,.F.);
#8328=ORIENTED_EDGE('',*,*,#5853,.F.);
#8329=ORIENTED_EDGE('',*,*,#5854,.F.);
#8330=ORIENTED_EDGE('',*,*,#5855,.F.);
#8331=ORIENTED_EDGE('',*,*,#5856,.F.);
#8332=ORIENTED_EDGE('',*,*,#5855,.T.);
#8333=ORIENTED_EDGE('',*,*,#5857,.T.);
#8334=ORIENTED_EDGE('',*,*,#5842,.T.);
#8335=ORIENTED_EDGE('',*,*,#5858,.T.);
#8336=ORIENTED_EDGE('',*,*,#5859,.F.);
#8337=ORIENTED_EDGE('',*,*,#5860,.F.);
#8338=ORIENTED_EDGE('',*,*,#5861,.F.);
#8339=ORIENTED_EDGE('',*,*,#5856,.T.);
#8340=ORIENTED_EDGE('',*,*,#5862,.T.);
#8341=ORIENTED_EDGE('',*,*,#5860,.T.);
#8342=ORIENTED_EDGE('',*,*,#5863,.T.);
#8343=ORIENTED_EDGE('',*,*,#5861,.T.);
#8344=ORIENTED_EDGE('',*,*,#5864,.T.);
#8345=ORIENTED_EDGE('',*,*,#5849,.T.);
#8346=ORIENTED_EDGE('',*,*,#5865,.T.);
#8347=ORIENTED_EDGE('',*,*,#5852,.T.);
#8348=ORIENTED_EDGE('',*,*,#5866,.T.);
#8349=ORIENTED_EDGE('',*,*,#5859,.T.);
#8350=ORIENTED_EDGE('',*,*,#5867,.T.);
#8351=ORIENTED_EDGE('',*,*,#5846,.T.);
#8352=ORIENTED_EDGE('',*,*,#5868,.T.);
#8353=ORIENTED_EDGE('',*,*,#5854,.T.);
#8354=ORIENTED_EDGE('',*,*,#5869,.T.);
#8355=ORIENTED_EDGE('',*,*,#5837,.T.);
#8356=ORIENTED_EDGE('',*,*,#5870,.T.);
#8357=ORIENTED_EDGE('',*,*,#5853,.T.);
#8358=ORIENTED_EDGE('',*,*,#5871,.T.);
#8359=ORIENTED_EDGE('',*,*,#5851,.T.);
#8360=ORIENTED_EDGE('',*,*,#5872,.T.);
#8361=ORIENTED_EDGE('',*,*,#5847,.T.);
#8362=ORIENTED_EDGE('',*,*,#5873,.T.);
#8363=ORIENTED_EDGE('',*,*,#5850,.T.);
#8364=ORIENTED_EDGE('',*,*,#5874,.T.);
#8365=ORIENTED_EDGE('',*,*,#5833,.T.);
#8366=ORIENTED_EDGE('',*,*,#5819,.T.);
#8367=ORIENTED_EDGE('',*,*,#5838,.T.);
#8368=ORIENTED_EDGE('',*,*,#5875,.T.);
#8369=ORIENTED_EDGE('',*,*,#5848,.T.);
#8370=ORIENTED_EDGE('',*,*,#5822,.T.);
#8371=ORIENTED_EDGE('',*,*,#5845,.T.);
#8372=ORIENTED_EDGE('',*,*,#5876,.T.);
#8373=ORIENTED_EDGE('',*,*,#5829,.T.);
#8374=ORIENTED_EDGE('',*,*,#5877,.T.);
#8375=ORIENTED_EDGE('',*,*,#5828,.T.);
#8376=ORIENTED_EDGE('',*,*,#5878,.T.);
#8377=ORIENTED_EDGE('',*,*,#5840,.T.);
#8378=ORIENTED_EDGE('',*,*,#5879,.T.);
#8379=ORIENTED_EDGE('',*,*,#5823,.T.);
#8380=ORIENTED_EDGE('',*,*,#5880,.T.);
#8381=ORIENTED_EDGE('',*,*,#5839,.T.);
#8382=ORIENTED_EDGE('',*,*,#5821,.T.);
#8383=ORIENTED_EDGE('',*,*,#5824,.T.);
#8384=ORIENTED_EDGE('',*,*,#5820,.T.);
#8385=ORIENTED_EDGE('',*,*,#5832,.T.);
#8386=ORIENTED_EDGE('',*,*,#5881,.T.);
#8387=ORIENTED_EDGE('',*,*,#5882,.T.);
#8388=ORIENTED_EDGE('',*,*,#5827,.T.);
#8389=ORIENTED_EDGE('',*,*,#5883,.T.);
#8390=ORIENTED_EDGE('',*,*,#5884,.T.);
#8391=ORIENTED_EDGE('',*,*,#5885,.T.);
#8392=ORIENTED_EDGE('',*,*,#5825,.T.);
#8393=ORIENTED_EDGE('',*,*,#5886,.T.);
#8394=ORIENTED_EDGE('',*,*,#5884,.F.);
#8395=ORIENTED_EDGE('',*,*,#5886,.F.);
#8396=ORIENTED_EDGE('',*,*,#5881,.F.);
#8397=ORIENTED_EDGE('',*,*,#5834,.F.);
#8398=ORIENTED_EDGE('',*,*,#5887,.T.);
#8399=ORIENTED_EDGE('',*,*,#5830,.F.);
#8400=ORIENTED_EDGE('',*,*,#5874,.F.);
#8401=ORIENTED_EDGE('',*,*,#5864,.F.);
#8402=ORIENTED_EDGE('',*,*,#5862,.F.);
#8403=ORIENTED_EDGE('',*,*,#5858,.F.);
#8404=ORIENTED_EDGE('',*,*,#5843,.F.);
#8405=ORIENTED_EDGE('',*,*,#5835,.F.);
#8406=ORIENTED_EDGE('',*,*,#5857,.F.);
#8407=ORIENTED_EDGE('',*,*,#5868,.F.);
#8408=ORIENTED_EDGE('',*,*,#5877,.F.);
#8409=ORIENTED_EDGE('',*,*,#5879,.F.);
#8410=ORIENTED_EDGE('',*,*,#5863,.F.);
#8411=ORIENTED_EDGE('',*,*,#5866,.F.);
#8412=ORIENTED_EDGE('',*,*,#5873,.F.);
#8413=ORIENTED_EDGE('',*,*,#5869,.F.);
#8414=ORIENTED_EDGE('',*,*,#5888,.F.);
#8415=ORIENTED_EDGE('',*,*,#5889,.F.);
#8416=ORIENTED_EDGE('',*,*,#5890,.F.);
#8417=ORIENTED_EDGE('',*,*,#5891,.F.);
#8418=ORIENTED_EDGE('',*,*,#5865,.F.);
#8419=ORIENTED_EDGE('',*,*,#5875,.F.);
#8420=ORIENTED_EDGE('',*,*,#5871,.F.);
#8421=ORIENTED_EDGE('',*,*,#5867,.F.);
#8422=ORIENTED_EDGE('',*,*,#5870,.F.);
#8423=ORIENTED_EDGE('',*,*,#5880,.F.);
#8424=ORIENTED_EDGE('',*,*,#5826,.F.);
#8425=ORIENTED_EDGE('',*,*,#5885,.F.);
#8426=ORIENTED_EDGE('',*,*,#5883,.F.);
#8427=ORIENTED_EDGE('',*,*,#5876,.F.);
#8428=ORIENTED_EDGE('',*,*,#5872,.F.);
#8429=ORIENTED_EDGE('',*,*,#5892,.T.);
#8430=ORIENTED_EDGE('',*,*,#5818,.T.);
#8431=ORIENTED_EDGE('',*,*,#5893,.T.);
#8432=ORIENTED_EDGE('',*,*,#5888,.T.);
#8433=ORIENTED_EDGE('',*,*,#5894,.T.);
#8434=ORIENTED_EDGE('',*,*,#5889,.T.);
#8435=ORIENTED_EDGE('',*,*,#5893,.F.);
#8436=ORIENTED_EDGE('',*,*,#5895,.T.);
#8437=ORIENTED_EDGE('',*,*,#5896,.T.);
#8438=ORIENTED_EDGE('',*,*,#5890,.T.);
#8439=ORIENTED_EDGE('',*,*,#5894,.F.);
#8440=ORIENTED_EDGE('',*,*,#5897,.T.);
#8441=ORIENTED_EDGE('',*,*,#5892,.F.);
#8442=ORIENTED_EDGE('',*,*,#5891,.T.);
#8443=ORIENTED_EDGE('',*,*,#5896,.F.);
#8444=ORIENTED_EDGE('',*,*,#5815,.T.);
#8445=ORIENTED_EDGE('',*,*,#5813,.F.);
#8446=ORIENTED_EDGE('',*,*,#5898,.F.);
#8447=ORIENTED_EDGE('',*,*,#5895,.F.);
#8448=ORIENTED_EDGE('',*,*,#5817,.T.);
#8449=ORIENTED_EDGE('',*,*,#5811,.F.);
#8450=ORIENTED_EDGE('',*,*,#5816,.F.);
#8451=ORIENTED_EDGE('',*,*,#5897,.F.);
#8452=ORIENTED_EDGE('',*,*,#5898,.T.);
#8453=ORIENTED_EDGE('',*,*,#5882,.F.);
#8454=ORIENTED_EDGE('',*,*,#5887,.F.);
#8455=ORIENTED_EDGE('',*,*,#5844,.F.);
#8456=ORIENTED_EDGE('',*,*,#5878,.F.);
#8981=PLANE('',#10729);
#8982=PLANE('',#10730);
#8983=PLANE('',#10792);
#8984=PLANE('',#10793);
#8985=PLANE('',#10794);
#8986=PLANE('',#10795);
#8987=PLANE('',#10798);
#8988=PLANE('',#10799);
#8989=PLANE('',#10810);
#8990=PLANE('',#10811);
#9480=ADVANCED_FACE('',(#2493),#569,.T.);
#9481=ADVANCED_FACE('',(#2494),#249,.T.);
#9482=ADVANCED_FACE('',(#2495),#570,.T.);
#9483=ADVANCED_FACE('',(#2496),#250,.T.);
#9484=ADVANCED_FACE('',(#2497),#571,.F.);
#9485=ADVANCED_FACE('',(#2498),#8981,.F.);
#9486=ADVANCED_FACE('',(#2499,#2020),#8982,.T.);
#9487=ADVANCED_FACE('',(#2500),#251,.T.);
#9488=ADVANCED_FACE('',(#2501),#187,.T.);
#9489=ADVANCED_FACE('',(#2502),#252,.T.);
#9490=ADVANCED_FACE('',(#2503),#572,.T.);
#9491=ADVANCED_FACE('',(#2504),#188,.T.);
#9492=ADVANCED_FACE('',(#2505),#189,.T.);
#9493=ADVANCED_FACE('',(#2506),#573,.T.);
#9494=ADVANCED_FACE('',(#2507),#190,.T.);
#9495=ADVANCED_FACE('',(#2508),#191,.T.);
#9496=ADVANCED_FACE('',(#2509),#192,.T.);
#9497=ADVANCED_FACE('',(#2510),#193,.T.);
#9498=ADVANCED_FACE('',(#2511),#574,.T.);
#9499=ADVANCED_FACE('',(#2512),#194,.T.);
#9500=ADVANCED_FACE('',(#2513),#575,.T.);
#9501=ADVANCED_FACE('',(#2514),#576,.T.);
#9502=ADVANCED_FACE('',(#2515),#577,.T.);
#9503=ADVANCED_FACE('',(#2516),#578,.T.);
#9504=ADVANCED_FACE('',(#2517),#579,.T.);
#9505=ADVANCED_FACE('',(#2518),#580,.T.);
#9506=ADVANCED_FACE('',(#2519),#581,.T.);
#9507=ADVANCED_FACE('',(#2520),#582,.T.);
#9508=ADVANCED_FACE('',(#2521),#583,.T.);
#9509=ADVANCED_FACE('',(#2522),#584,.T.);
#9510=ADVANCED_FACE('',(#2523),#585,.T.);
#9511=ADVANCED_FACE('',(#2524),#586,.F.);
#9512=ADVANCED_FACE('',(#2525),#587,.T.);
#9513=ADVANCED_FACE('',(#2526),#588,.T.);
#9514=ADVANCED_FACE('',(#2527),#8983,.T.);
#9515=ADVANCED_FACE('',(#2528),#8984,.F.);
#9516=ADVANCED_FACE('',(#2529),#8985,.T.);
#9517=ADVANCED_FACE('',(#2530,#2021),#8986,.T.);
#9518=ADVANCED_FACE('',(#2531),#8987,.T.);
#9519=ADVANCED_FACE('',(#2532),#8988,.T.);
#9520=ADVANCED_FACE('',(#2533),#589,.T.);
#9521=ADVANCED_FACE('',(#2534),#253,.T.);
#9522=ADVANCED_FACE('',(#2535),#590,.T.);
#9523=ADVANCED_FACE('',(#2536),#254,.T.);
#9524=ADVANCED_FACE('',(#2537),#591,.F.);
#9525=ADVANCED_FACE('',(#2538),#8989,.F.);
#9526=ADVANCED_FACE('',(#2539),#8990,.T.);
#9634=CLOSED_SHELL('',(#9480,#9481,#9482,#9483,#9484,#9485,#9486,#9487,
#9488,#9489,#9490,#9491,#9492,#9493,#9494,#9495,#9496,#9497,#9498,#9499,
#9500,#9501,#9502,#9503,#9504,#9505,#9506,#9507,#9508,#9509,#9510,#9511,
#9512,#9513,#9514,#9515,#9516,#9517,#9518,#9519,#9520,#9521,#9522,#9523,
#9524,#9525,#9526));
#10714=AXIS2_PLACEMENT_3D('',#17188,#13482,#13483);
#10715=AXIS2_PLACEMENT_3D('',#17189,#13484,#13485);
#10716=AXIS2_PLACEMENT_3D('',#17192,#13486,#13487);
#10717=AXIS2_PLACEMENT_3D('',#17196,#13489,#13490);
#10718=AXIS2_PLACEMENT_3D('',#17198,#13492,#13493);
#10719=AXIS2_PLACEMENT_3D('',#17201,#13494,#13495);
#10720=AXIS2_PLACEMENT_3D('',#17202,#13496,#13497);
#10721=AXIS2_PLACEMENT_3D('',#17203,#13498,#13499);
#10722=AXIS2_PLACEMENT_3D('',#17204,#13500,#13501);
#10723=AXIS2_PLACEMENT_3D('',#17207,#13502,#13503);
#10724=AXIS2_PLACEMENT_3D('',#17210,#13506,#13507);
#10725=AXIS2_PLACEMENT_3D('',#17211,#13508,#13509);
#10726=AXIS2_PLACEMENT_3D('',#17212,#13510,#13511);
#10727=AXIS2_PLACEMENT_3D('',#17213,#13512,#13513);
#10728=AXIS2_PLACEMENT_3D('',#17217,#13515,#13516);
#10729=AXIS2_PLACEMENT_3D('',#17219,#13518,#13519);
#10730=AXIS2_PLACEMENT_3D('',#17223,#13522,#13523);
#10731=AXIS2_PLACEMENT_3D('',#17232,#13528,#13529);
#10732=AXIS2_PLACEMENT_3D('',#17234,#13530,#13531);
#10733=AXIS2_PLACEMENT_3D('',#17236,#13532,#13533);
#10734=AXIS2_PLACEMENT_3D('',#17238,#13534,#13535);
#10735=AXIS2_PLACEMENT_3D('',#17239,#13536,#13537);
#10736=AXIS2_PLACEMENT_3D('',#17240,#13538,#13539);
#10737=AXIS2_PLACEMENT_3D('',#17243,#13540,#13541);
#10738=AXIS2_PLACEMENT_3D('',#17245,#13542,#13543);
#10739=AXIS2_PLACEMENT_3D('',#17246,#13544,#13545);
#10740=AXIS2_PLACEMENT_3D('',#17247,#13546,#13547);
#10741=AXIS2_PLACEMENT_3D('',#17250,#13548,#13549);
#10742=AXIS2_PLACEMENT_3D('',#17252,#13550,#13551);
#10743=AXIS2_PLACEMENT_3D('',#17253,#13552,#13553);
#10744=AXIS2_PLACEMENT_3D('',#17254,#13554,#13555);
#10745=AXIS2_PLACEMENT_3D('',#17255,#13556,#13557);
#10746=AXIS2_PLACEMENT_3D('',#17260,#13560,#13561);
#10747=AXIS2_PLACEMENT_3D('',#17261,#13562,#13563);
#10748=AXIS2_PLACEMENT_3D('',#17264,#13564,#13565);
#10749=AXIS2_PLACEMENT_3D('',#17265,#13566,#13567);
#10750=AXIS2_PLACEMENT_3D('',#17266,#13568,#13569);
#10751=AXIS2_PLACEMENT_3D('',#17267,#13570,#13571);
#10752=AXIS2_PLACEMENT_3D('',#17270,#13572,#13573);
#10753=AXIS2_PLACEMENT_3D('',#17272,#13574,#13575);
#10754=AXIS2_PLACEMENT_3D('',#17273,#13576,#13577);
#10755=AXIS2_PLACEMENT_3D('',#17274,#13578,#13579);
#10756=AXIS2_PLACEMENT_3D('',#17277,#13582,#13583);
#10757=AXIS2_PLACEMENT_3D('',#17280,#13584,#13585);
#10758=AXIS2_PLACEMENT_3D('',#17282,#13586,#13587);
#10759=AXIS2_PLACEMENT_3D('',#17283,#13588,#13589);
#10760=AXIS2_PLACEMENT_3D('',#17284,#13590,#13591);
#10761=AXIS2_PLACEMENT_3D('',#17286,#13592,#13593);
#10762=AXIS2_PLACEMENT_3D('',#17288,#13594,#13595);
#10763=AXIS2_PLACEMENT_3D('',#17289,#13596,#13597);
#10764=AXIS2_PLACEMENT_3D('',#17290,#13598,#13599);
#10765=AXIS2_PLACEMENT_3D('',#17293,#13600,#13601);
#10766=AXIS2_PLACEMENT_3D('',#17295,#13602,#13603);
#10767=AXIS2_PLACEMENT_3D('',#17296,#13604,#13605);
#10768=AXIS2_PLACEMENT_3D('',#17297,#13606,#13607);
#10769=AXIS2_PLACEMENT_3D('',#17300,#13608,#13609);
#10770=AXIS2_PLACEMENT_3D('',#17302,#13610,#13611);
#10771=AXIS2_PLACEMENT_3D('',#17303,#13612,#13613);
#10772=AXIS2_PLACEMENT_3D('',#17304,#13614,#13615);
#10773=AXIS2_PLACEMENT_3D('',#17307,#13618,#13619);
#10774=AXIS2_PLACEMENT_3D('',#17310,#13620,#13621);
#10775=AXIS2_PLACEMENT_3D('',#17312,#13622,#13623);
#10776=AXIS2_PLACEMENT_3D('',#17313,#13624,#13625);
#10777=AXIS2_PLACEMENT_3D('',#17314,#13626,#13627);
#10778=AXIS2_PLACEMENT_3D('',#17317,#13630,#13631);
#10779=AXIS2_PLACEMENT_3D('',#17320,#13634,#13635);
#10780=AXIS2_PLACEMENT_3D('',#17323,#13638,#13639);
#10781=AXIS2_PLACEMENT_3D('',#17326,#13642,#13643);
#10782=AXIS2_PLACEMENT_3D('',#17329,#13646,#13647);
#10783=AXIS2_PLACEMENT_3D('',#17332,#13650,#13651);
#10784=AXIS2_PLACEMENT_3D('',#17334,#13653,#13654);
#10785=AXIS2_PLACEMENT_3D('',#17336,#13656,#13657);
#10786=AXIS2_PLACEMENT_3D('',#17339,#13660,#13661);
#10787=AXIS2_PLACEMENT_3D('',#17342,#13664,#13665);
#10788=AXIS2_PLACEMENT_3D('',#17344,#13667,#13668);
#10789=AXIS2_PLACEMENT_3D('',#17346,#13670,#13671);
#10790=AXIS2_PLACEMENT_3D('',#17351,#13674,#13675);
#10791=AXIS2_PLACEMENT_3D('',#17352,#13676,#13677);
#10792=AXIS2_PLACEMENT_3D('',#17355,#13680,#13681);
#10793=AXIS2_PLACEMENT_3D('',#17357,#13683,#13684);
#10794=AXIS2_PLACEMENT_3D('',#17358,#13685,#13686);
#10795=AXIS2_PLACEMENT_3D('',#17359,#13687,#13688);
#10796=AXIS2_PLACEMENT_3D('',#17364,#13690,#13691);
#10797=AXIS2_PLACEMENT_3D('',#17367,#13693,#13694);
#10798=AXIS2_PLACEMENT_3D('',#17368,#13695,#13696);
#10799=AXIS2_PLACEMENT_3D('',#17369,#13697,#13698);
#10800=AXIS2_PLACEMENT_3D('',#17370,#13699,#13700);
#10801=AXIS2_PLACEMENT_3D('',#17371,#13701,#13702);
#10802=AXIS2_PLACEMENT_3D('',#17372,#13703,#13704);
#10803=AXIS2_PLACEMENT_3D('',#17373,#13705,#13706);
#10804=AXIS2_PLACEMENT_3D('',#17375,#13707,#13708);
#10805=AXIS2_PLACEMENT_3D('',#17376,#13709,#13710);
#10806=AXIS2_PLACEMENT_3D('',#17377,#13711,#13712);
#10807=AXIS2_PLACEMENT_3D('',#17378,#13713,#13714);
#10808=AXIS2_PLACEMENT_3D('',#17380,#13716,#13717);
#10809=AXIS2_PLACEMENT_3D('',#17381,#13718,#13719);
#10810=AXIS2_PLACEMENT_3D('',#17383,#13721,#13722);
#10811=AXIS2_PLACEMENT_3D('',#17384,#13723,#13724);
#13482=DIRECTION('axis',(0.,0.,1.));
#13483=DIRECTION('refdir',(1.,0.,0.));
#13484=DIRECTION('center_axis',(1.,0.,0.));
#13485=DIRECTION('ref_axis',(0.,0.707106781186519,-0.707106781186576));
#13486=DIRECTION('center_axis',(1.,0.,0.));
#13487=DIRECTION('ref_axis',(0.,0.,-1.));
#13488=DIRECTION('',(1.,0.,0.));
#13489=DIRECTION('center_axis',(-1.,0.,0.));
#13490=DIRECTION('ref_axis',(0.,1.,0.));
#13491=DIRECTION('',(-1.,0.,0.));
#13492=DIRECTION('center_axis',(0.,0.,1.));
#13493=DIRECTION('ref_axis',(1.,0.,0.));
#13494=DIRECTION('center_axis',(1.,0.,0.));
#13495=DIRECTION('ref_axis',(0.,-1.,0.));
#13496=DIRECTION('center_axis',(0.,0.,-1.));
#13497=DIRECTION('ref_axis',(1.,0.,0.));
#13498=DIRECTION('center_axis',(0.,0.,1.));
#13499=DIRECTION('ref_axis',(1.,0.,0.));
#13500=DIRECTION('center_axis',(-1.,0.,0.));
#13501=DIRECTION('ref_axis',(0.,-0.707106781186561,-0.707106781186534));
#13502=DIRECTION('center_axis',(1.,0.,0.));
#13503=DIRECTION('ref_axis',(0.,-1.,0.));
#13504=DIRECTION('',(1.,0.,0.));
#13505=DIRECTION('',(-1.,0.,0.));
#13506=DIRECTION('center_axis',(0.,0.,1.));
#13507=DIRECTION('ref_axis',(-1.,0.,0.));
#13508=DIRECTION('center_axis',(0.,0.,-1.));
#13509=DIRECTION('ref_axis',(-1.,0.,0.));
#13510=DIRECTION('center_axis',(0.,0.,1.));
#13511=DIRECTION('ref_axis',(-1.,0.,0.));
#13512=DIRECTION('center_axis',(0.,0.,-1.));
#13513=DIRECTION('ref_axis',(0.,-1.,0.));
#13514=DIRECTION('',(0.,0.,-1.));
#13515=DIRECTION('center_axis',(0.,0.,-1.));
#13516=DIRECTION('ref_axis',(1.,0.,0.));
#13517=DIRECTION('',(0.,0.,-1.));
#13518=DIRECTION('center_axis',(0.,-1.,0.));
#13519=DIRECTION('ref_axis',(-1.,0.,0.));
#13520=DIRECTION('',(0.,0.,-1.));
#13521=DIRECTION('',(-1.,0.,0.));
#13522=DIRECTION('center_axis',(0.,0.,-1.));
#13523=DIRECTION('ref_axis',(-1.,0.,0.));
#13524=DIRECTION('',(1.,0.,0.));
#13525=DIRECTION('',(0.,-1.,0.));
#13526=DIRECTION('',(-1.,0.,0.));
#13527=DIRECTION('',(0.,1.,0.));
#13528=DIRECTION('center_axis',(0.,-1.,0.));
#13529=DIRECTION('ref_axis',(0.,0.,-1.));
#13530=DIRECTION('center_axis',(1.,0.,0.));
#13531=DIRECTION('ref_axis',(0.,0.,-1.));
#13532=DIRECTION('center_axis',(0.,-1.,0.));
#13533=DIRECTION('ref_axis',(-1.,0.,0.));
#13534=DIRECTION('center_axis',(0.,0.,-1.));
#13535=DIRECTION('ref_axis',(0.,1.,0.));
#13536=DIRECTION('center_axis',(0.,1.,0.));
#13537=DIRECTION('ref_axis',(-0.70710678118654,0.,0.707106781186555));
#13538=DIRECTION('center_axis',(-0.816496580927734,-0.408248290463867,0.408248290463843));
#13539=DIRECTION('ref_axis',(-0.577350269189598,0.577350269189645,-0.577350269189634));
#13540=DIRECTION('center_axis',(-1.,0.,0.));
#13541=DIRECTION('ref_axis',(0.,0.,-1.));
#13542=DIRECTION('center_axis',(0.,1.,0.));
#13543=DIRECTION('ref_axis',(-1.,0.,0.));
#13544=DIRECTION('center_axis',(-9.25185853854317E-16,0.,-1.));
#13545=DIRECTION('ref_axis',(0.,1.,0.));
#13546=DIRECTION('center_axis',(0.,-1.,0.));
#13547=DIRECTION('ref_axis',(0.,0.,-1.));
#13548=DIRECTION('center_axis',(0.,-1.,0.));
#13549=DIRECTION('ref_axis',(-0.70710678118654,0.,0.707106781186555));
#13550=DIRECTION('center_axis',(0.,0.,-1.));
#13551=DIRECTION('ref_axis',(1.,0.,0.));
#13552=DIRECTION('center_axis',(-5.92118946466763E-14,1.,0.));
#13553=DIRECTION('ref_axis',(0.,0.,1.));
#13554=DIRECTION('center_axis',(1.,0.,0.));
#13555=DIRECTION('ref_axis',(0.,-1.,0.));
#13556=DIRECTION('center_axis',(0.,0.,-1.));
#13557=DIRECTION('ref_axis',(0.707106781186547,-0.707106781186547,0.));
#13558=DIRECTION('',(0.,0.,1.));
#13559=DIRECTION('',(0.,0.,-1.));
#13560=DIRECTION('center_axis',(0.707106781186576,0.,0.707106781186519));
#13561=DIRECTION('ref_axis',(-0.707106781186519,0.,0.707106781186576));
#13562=DIRECTION('center_axis',(-0.827465426020362,0.538877990790925,-0.157833709270471));
#13563=DIRECTION('ref_axis',(0.561516668266355,0.794104487760816,-0.232587819494453));
#13564=DIRECTION('center_axis',(0.707106781186544,-3.663549070262E-14,-0.707106781186551));
#13565=DIRECTION('ref_axis',(0.707106781186551,0.,0.707106781186544));
#13566=DIRECTION('center_axis',(0.,1.,0.));
#13567=DIRECTION('ref_axis',(0.,0.,-1.));
#13568=DIRECTION('center_axis',(1.,0.,-2.96059473233375E-14));
#13569=DIRECTION('ref_axis',(0.,1.,0.));
#13570=DIRECTION('center_axis',(0.408248290463871,0.408248290463824,-0.816496580927742));
#13571=DIRECTION('ref_axis',(-0.577350269189681,-0.577350269189586,-0.57735026918961));
#13572=DIRECTION('center_axis',(0.,-1.,0.));
#13573=DIRECTION('ref_axis',(0.,0.,-1.));
#13574=DIRECTION('center_axis',(-1.,0.,5.9211894646675E-14));
#13575=DIRECTION('ref_axis',(0.,-1.,0.));
#13576=DIRECTION('center_axis',(0.,-9.25185853854317E-16,-1.));
#13577=DIRECTION('ref_axis',(-1.,0.,0.));
#13578=DIRECTION('center_axis',(-1.,0.,0.));
#13579=DIRECTION('ref_axis',(0.,-0.707106781186519,-0.707106781186576));
#13580=DIRECTION('',(-1.,0.,0.));
#13581=DIRECTION('',(1.,0.,0.));
#13582=DIRECTION('center_axis',(-0.408248290463863,0.408248290463816,-0.81649658092775));
#13583=DIRECTION('ref_axis',(-0.577350269189665,0.577350269189618,0.577350269189594));
#13584=DIRECTION('center_axis',(0.,0.,1.));
#13585=DIRECTION('ref_axis',(-1.,0.,0.));
#13586=DIRECTION('center_axis',(0.,1.,0.));
#13587=DIRECTION('ref_axis',(0.,0.,1.));
#13588=DIRECTION('center_axis',(-1.,0.,5.9211894646675E-14));
#13589=DIRECTION('ref_axis',(0.,1.,0.));
#13590=DIRECTION('center_axis',(-0.827465426020388,-0.538877990790895,-0.157833709270442));
#13591=DIRECTION('ref_axis',(0.561516668266318,-0.794104487760845,-0.232587819494444));
#13592=DIRECTION('center_axis',(0.,-1.,0.));
#13593=DIRECTION('ref_axis',(0.707106781186544,0.,0.707106781186551));
#13594=DIRECTION('center_axis',(0.70710678118657,0.,-0.707106781186525));
#13595=DIRECTION('ref_axis',(0.,-1.,0.));
#13596=DIRECTION('center_axis',(1.,2.96059473233364E-14,0.));
#13597=DIRECTION('ref_axis',(0.,0.,-1.));
#13598=DIRECTION('center_axis',(0.182143211721525,-0.8794652240646,0.439732612032324));
#13599=DIRECTION('ref_axis',(0.336556770590774,0.475963149478001,0.812519920068728));
#13600=DIRECTION('center_axis',(1.,0.,0.));
#13601=DIRECTION('ref_axis',(0.,0.,1.));
#13602=DIRECTION('center_axis',(0.,1.,0.));
#13603=DIRECTION('ref_axis',(0.707106781186551,0.,0.707106781186544));
#13604=DIRECTION('center_axis',(-0.70710678118654,0.,0.707106781186555));
#13605=DIRECTION('ref_axis',(0.,1.,0.));
#13606=DIRECTION('center_axis',(-0.408248290463908,-0.408248290463861,-0.816496580927704));
#13607=DIRECTION('ref_axis',(-0.577350269189642,-0.577350269189594,0.577350269189642));
#13608=DIRECTION('center_axis',(0.,-1.,5.9211894646675E-14));
#13609=DIRECTION('ref_axis',(-1.,0.,0.));
#13610=DIRECTION('center_axis',(0.,0.,1.));
#13611=DIRECTION('ref_axis',(0.,-1.,0.));
#13612=DIRECTION('center_axis',(-1.,0.,0.));
#13613=DIRECTION('ref_axis',(0.,0.,1.));
#13614=DIRECTION('center_axis',(0.,0.,1.));
#13615=DIRECTION('ref_axis',(-0.707106781186589,-0.707106781186506,0.));
#13616=DIRECTION('',(0.,0.,-1.));
#13617=DIRECTION('',(0.,0.,1.));
#13618=DIRECTION('center_axis',(-0.182143211721517,-0.879465224064606,-0.439732612032315));
#13619=DIRECTION('ref_axis',(0.336556770590767,-0.475963149477992,0.812519920068736));
#13620=DIRECTION('center_axis',(0.,-1.,0.));
#13621=DIRECTION('ref_axis',(0.,0.,1.));
#13622=DIRECTION('center_axis',(1.,0.,0.));
#13623=DIRECTION('ref_axis',(0.,-1.,0.));
#13624=DIRECTION('center_axis',(-0.70710678118654,0.,0.707106781186555));
#13625=DIRECTION('ref_axis',(0.707106781186555,0.,0.70710678118654));
#13626=DIRECTION('center_axis',(-1.,0.,0.));
#13627=DIRECTION('ref_axis',(0.,-0.707106781186558,0.707106781186537));
#13628=DIRECTION('',(1.,0.,0.));
#13629=DIRECTION('',(-1.,0.,0.));
#13630=DIRECTION('center_axis',(-0.707106781186547,0.,0.707106781186548));
#13631=DIRECTION('ref_axis',(0.499999999999997,-0.707106781186559,0.499999999999986));
#13632=DIRECTION('',(0.707106781186547,0.,-0.707106781186548));
#13633=DIRECTION('',(-0.707106781186547,0.,0.707106781186548));
#13634=DIRECTION('center_axis',(0.,1.,0.));
#13635=DIRECTION('ref_axis',(0.382683432365094,0.,0.923879532511285));
#13636=DIRECTION('',(0.,-1.,0.));
#13637=DIRECTION('',(0.,1.,0.));
#13638=DIRECTION('center_axis',(0.,1.,0.));
#13639=DIRECTION('ref_axis',(-0.707106781186558,0.,0.707106781186537));
#13640=DIRECTION('',(0.,-1.,0.));
#13641=DIRECTION('',(0.,1.,0.));
#13642=DIRECTION('center_axis',(0.707106781186547,0.,-0.707106781186548));
#13643=DIRECTION('ref_axis',(0.499999999999997,0.707106781186559,0.499999999999986));
#13644=DIRECTION('',(-0.707106781186547,0.,0.707106781186548));
#13645=DIRECTION('',(0.707106781186547,0.,-0.707106781186548));
#13646=DIRECTION('center_axis',(1.,0.,0.));
#13647=DIRECTION('ref_axis',(0.,0.707106781186558,0.707106781186537));
#13648=DIRECTION('',(-1.,0.,0.));
#13649=DIRECTION('',(1.,0.,0.));
#13650=DIRECTION('center_axis',(1.,0.,0.));
#13651=DIRECTION('ref_axis',(0.,-0.707106781186561,-0.707106781186534));
#13652=DIRECTION('',(-1.,0.,0.));
#13653=DIRECTION('center_axis',(0.,1.,0.));
#13654=DIRECTION('ref_axis',(0.923879532511297,0.,-0.382683432365066));
#13655=DIRECTION('',(0.,-1.,0.));
#13656=DIRECTION('center_axis',(0.,0.,1.));
#13657=DIRECTION('ref_axis',(-0.707106781186506,0.707106781186589,0.));
#13658=DIRECTION('',(0.,0.,-1.));
#13659=DIRECTION('',(0.,0.,1.));
#13660=DIRECTION('center_axis',(0.,1.,0.));
#13661=DIRECTION('ref_axis',(-0.707106781186519,0.,-0.707106781186576));
#13662=DIRECTION('',(0.,-1.,0.));
#13663=DIRECTION('',(0.,1.,0.));
#13664=DIRECTION('center_axis',(-1.,0.,0.));
#13665=DIRECTION('ref_axis',(0.,0.707106781186561,-0.707106781186534));
#13666=DIRECTION('',(1.,0.,0.));
#13667=DIRECTION('center_axis',(0.,1.,0.));
#13668=DIRECTION('ref_axis',(-0.707106781186519,0.,0.707106781186576));
#13669=DIRECTION('',(0.,1.,0.));
#13670=DIRECTION('center_axis',(-1.,0.,0.));
#13671=DIRECTION('ref_axis',(0.,0.707106781186561,-0.707106781186534));
#13672=DIRECTION('',(-1.,0.,0.));
#13673=DIRECTION('',(1.,0.,0.));
#13674=DIRECTION('center_axis',(-0.707106781186555,0.,-0.70710678118654));
#13675=DIRECTION('ref_axis',(0.70710678118654,0.,-0.707106781186555));
#13676=DIRECTION('center_axis',(0.,0.,-1.));
#13677=DIRECTION('ref_axis',(0.707106781186506,0.707106781186589,0.));
#13678=DIRECTION('',(0.,0.,1.));
#13679=DIRECTION('',(0.,0.,-1.));
#13680=DIRECTION('center_axis',(1.,0.,0.));
#13681=DIRECTION('ref_axis',(0.,0.,-1.));
#13682=DIRECTION('',(0.,1.,0.));
#13683=DIRECTION('center_axis',(0.,1.,0.));
#13684=DIRECTION('ref_axis',(1.,0.,0.));
#13685=DIRECTION('center_axis',(-1.,0.,0.));
#13686=DIRECTION('ref_axis',(0.,0.,1.));
#13687=DIRECTION('center_axis',(0.,0.,1.));
#13688=DIRECTION('ref_axis',(1.,0.,0.));
#13689=DIRECTION('',(1.,0.,0.));
#13690=DIRECTION('center_axis',(0.,0.,1.));
#13691=DIRECTION('ref_axis',(-1.,0.,0.));
#13692=DIRECTION('',(-1.,0.,0.));
#13693=DIRECTION('center_axis',(0.,0.,1.));
#13694=DIRECTION('ref_axis',(1.,0.,0.));
#13695=DIRECTION('center_axis',(0.707106781186548,0.,0.707106781186547));
#13696=DIRECTION('ref_axis',(0.707106781186547,0.,-0.707106781186548));
#13697=DIRECTION('center_axis',(0.,1.,0.));
#13698=DIRECTION('ref_axis',(0.,0.,1.));
#13699=DIRECTION('center_axis',(-1.,0.,0.));
#13700=DIRECTION('ref_axis',(0.,0.707106781186516,0.707106781186579));
#13701=DIRECTION('center_axis',(-1.,0.,0.));
#13702=DIRECTION('ref_axis',(0.,0.,1.));
#13703=DIRECTION('center_axis',(1.,0.,0.));
#13704=DIRECTION('ref_axis',(0.,1.,0.));
#13705=DIRECTION('center_axis',(0.,0.,-1.));
#13706=DIRECTION('ref_axis',(-1.,0.,0.));
#13707=DIRECTION('center_axis',(-1.,0.,0.));
#13708=DIRECTION('ref_axis',(0.,-1.,0.));
#13709=DIRECTION('center_axis',(0.,0.,-1.));
#13710=DIRECTION('ref_axis',(-1.,0.,0.));
#13711=DIRECTION('center_axis',(1.,0.,0.));
#13712=DIRECTION('ref_axis',(0.,-0.707106781186558,0.707106781186537));
#13713=DIRECTION('center_axis',(-1.,0.,0.));
#13714=DIRECTION('ref_axis',(0.,-1.,0.));
#13715=DIRECTION('',(1.,0.,0.));
#13716=DIRECTION('center_axis',(0.,0.,-1.));
#13717=DIRECTION('ref_axis',(1.,0.,0.));
#13718=DIRECTION('center_axis',(0.,0.,-1.));
#13719=DIRECTION('ref_axis',(0.,1.,0.));
#13720=DIRECTION('',(0.,0.,-1.));
#13721=DIRECTION('center_axis',(0.,1.,0.));
#13722=DIRECTION('ref_axis',(1.,0.,0.));
#13723=DIRECTION('center_axis',(0.,0.,-1.));
#13724=DIRECTION('ref_axis',(-1.,0.,0.));
#17188=CARTESIAN_POINT('',(0.,0.,0.));
#17189=CARTESIAN_POINT('Origin',(-69.9040264336917,-84.8,3.08953555269655));
#17190=CARTESIAN_POINT('',(-104.475451921837,-84.8,2.78953555269655));
#17191=CARTESIAN_POINT('',(-104.475451921837,-84.5,3.08953555269655));
#17192=CARTESIAN_POINT('Origin',(-104.475451921837,-84.8,3.08953555269655));
#17193=CARTESIAN_POINT('',(-77.8080528673835,-84.5,3.08953555269655));
#17194=CARTESIAN_POINT('',(-69.9040264336917,-84.5,3.08953555269655));
#17195=CARTESIAN_POINT('',(-77.8080528673835,-84.8,2.78953555269655));
#17196=CARTESIAN_POINT('Origin',(-77.8080528673835,-84.8,3.08953555269655));
#17197=CARTESIAN_POINT('',(-69.9040264336917,-84.8,2.78953555269655));
#17198=CARTESIAN_POINT('Origin',(-77.8080528673835,-80.,3.08953555269655));
#17199=CARTESIAN_POINT('',(-77.8080528673835,-75.5,3.08953555269655));
#17200=CARTESIAN_POINT('',(-77.8080528673835,-75.2,2.78953555269655));
#17201=CARTESIAN_POINT('Origin',(-77.8080528673835,-75.2,3.08953555269655));
#17202=CARTESIAN_POINT('Origin',(-77.8080528673835,-80.,2.78953555269655));
#17203=CARTESIAN_POINT('Origin',(-77.8080528673835,-80.,3.08953555269655));
#17204=CARTESIAN_POINT('Origin',(-83.2377259609183,-75.2,3.08953555269655));
#17205=CARTESIAN_POINT('',(-104.475451921837,-75.5,3.08953555269655));
#17206=CARTESIAN_POINT('',(-104.475451921837,-75.2,2.78953555269655));
#17207=CARTESIAN_POINT('Origin',(-104.475451921837,-75.2,3.08953555269655));
#17208=CARTESIAN_POINT('',(-83.2377259609183,-75.2,2.78953555269655));
#17209=CARTESIAN_POINT('',(-83.2377259609183,-75.5,3.08953555269655));
#17210=CARTESIAN_POINT('Origin',(-104.475451921837,-80.,3.08953555269655));
#17211=CARTESIAN_POINT('Origin',(-104.475451921837,-80.,2.78953555269655));
#17212=CARTESIAN_POINT('Origin',(-104.475451921837,-80.,3.08953555269655));
#17213=CARTESIAN_POINT('Origin',(-77.8080528673835,-80.,10.7895355526966));
#17214=CARTESIAN_POINT('',(-77.8080528673835,-84.5,10.4895355526966));
#17215=CARTESIAN_POINT('',(-77.8080528673835,-84.5,10.7895355526966));
#17216=CARTESIAN_POINT('',(-77.8080528673835,-75.5,10.4895355526966));
#17217=CARTESIAN_POINT('Origin',(-77.8080528673835,-80.,10.4895355526966));
#17218=CARTESIAN_POINT('',(-77.8080528673835,-75.5,10.7895355526966));
#17219=CARTESIAN_POINT('Origin',(-77.8080528673835,-84.5,10.7895355526966));
#17220=CARTESIAN_POINT('',(-104.475451921837,-84.5,10.4895355526966));
#17221=CARTESIAN_POINT('',(-104.475451921837,-84.5,10.7895355526966));
#17222=CARTESIAN_POINT('',(-94.9040264336917,-84.5,10.4895355526966));
#17223=CARTESIAN_POINT('Origin',(-62.,-90.,2.78953555269655));
#17224=CARTESIAN_POINT('',(-109.7,-89.7,2.78953555269655));
#17225=CARTESIAN_POINT('',(-62.7242640687119,-89.7,2.78953555269655));
#17226=CARTESIAN_POINT('',(-74.5,-89.7,2.78953555269655));
#17227=CARTESIAN_POINT('',(-109.7,-70.3,2.78953555269655));
#17228=CARTESIAN_POINT('',(-109.7,-90.,2.78953555269655));
#17229=CARTESIAN_POINT('',(-62.7242640687119,-70.3,2.78953555269655));
#17230=CARTESIAN_POINT('',(-74.5,-70.3,2.78953555269655));
#17231=CARTESIAN_POINT('',(-62.7242640687119,-90.,2.78953555269655));
#17232=CARTESIAN_POINT('Origin',(-109.7,-70.3,2.48953555269655));
#17233=CARTESIAN_POINT('',(-109.7,-70.,3.08953555269655));
#17234=CARTESIAN_POINT('Origin',(-109.7,-70.3,3.08953555269655));
#17235=CARTESIAN_POINT('',(-110.,-70.3,2.48953555269655));
#17236=CARTESIAN_POINT('Origin',(-109.7,-70.3,2.48953555269655));
#17237=CARTESIAN_POINT('',(-110.3,-70.,2.48953555269655));
#17238=CARTESIAN_POINT('Origin',(-110.3,-70.3,2.48953555269655));
#17239=CARTESIAN_POINT('Origin',(-109.7,-70.,2.48953555269655));
#17240=CARTESIAN_POINT('Origin',(-111.7,-70.3,0.3));
#17241=CARTESIAN_POINT('',(-111.7,-70.3,0.));
#17242=CARTESIAN_POINT('',(-111.7,-70.,0.3));
#17243=CARTESIAN_POINT('Origin',(-111.7,-70.3,0.3));
#17244=CARTESIAN_POINT('',(-112.,-70.3,0.3));
#17245=CARTESIAN_POINT('Origin',(-111.7,-70.3,0.3));
#17246=CARTESIAN_POINT('Origin',(-111.7,-70.3,0.3));
#17247=CARTESIAN_POINT('Origin',(-109.7,-89.7,2.48953555269655));
#17248=CARTESIAN_POINT('',(-109.7,-90.,3.08953555269655));
#17249=CARTESIAN_POINT('',(-110.3,-90.,2.48953555269655));
#17250=CARTESIAN_POINT('Origin',(-109.7,-90.,2.48953555269655));
#17251=CARTESIAN_POINT('',(-110.,-89.7,2.48953555269655));
#17252=CARTESIAN_POINT('Origin',(-110.3,-89.7,2.48953555269655));
#17253=CARTESIAN_POINT('Origin',(-109.7,-89.7,2.48953555269655));
#17254=CARTESIAN_POINT('Origin',(-109.7,-89.7,3.08953555269655));
#17255=CARTESIAN_POINT('Origin',(-110.3,-89.7,4.09215166452241));
#17256=CARTESIAN_POINT('',(-110.,-89.7,0.));
#17257=CARTESIAN_POINT('',(-110.,-89.7,4.09215166452241));
#17258=CARTESIAN_POINT('',(-110.3,-90.,0.3));
#17259=CARTESIAN_POINT('',(-110.3,-90.,4.09215166452241));
#17260=CARTESIAN_POINT('Origin',(-110.3,-89.7,0.3));
#17261=CARTESIAN_POINT('Origin',(-62.7242640687119,-70.3,3.08953555269655));
#17262=CARTESIAN_POINT('',(-62.512132034356,-70.3,3.30166758705252));
#17263=CARTESIAN_POINT('',(-62.7242640687119,-70.,3.08953555269655));
#17264=CARTESIAN_POINT('Origin',(-62.7242640687119,-70.3,3.08953555269656));
#17265=CARTESIAN_POINT('Origin',(-62.7242640687119,-70.3,3.08953555269655));
#17266=CARTESIAN_POINT('Origin',(-62.7242640687119,-70.3,3.08953555269655));
#17267=CARTESIAN_POINT('Origin',(-111.7,-89.7,0.3));
#17268=CARTESIAN_POINT('',(-111.7,-89.7,0.));
#17269=CARTESIAN_POINT('',(-112.,-89.7,0.3));
#17270=CARTESIAN_POINT('Origin',(-111.7,-89.7,0.3));
#17271=CARTESIAN_POINT('',(-111.7,-90.,0.3));
#17272=CARTESIAN_POINT('Origin',(-111.7,-89.7,0.3));
#17273=CARTESIAN_POINT('Origin',(-111.7,-89.7,0.3));
#17274=CARTESIAN_POINT('Origin',(-98.5,-89.7,0.3));
#17275=CARTESIAN_POINT('',(-98.5,-90.,0.3));
#17276=CARTESIAN_POINT('',(-98.5,-89.7,0.));
#17277=CARTESIAN_POINT('Origin',(-111.7,-70.3,10.4895355526966));
#17278=CARTESIAN_POINT('',(-112.,-70.3,10.4895355526966));
#17279=CARTESIAN_POINT('',(-111.7,-70.,10.4895355526966));
#17280=CARTESIAN_POINT('Origin',(-111.7,-70.3,10.4895355526966));
#17281=CARTESIAN_POINT('',(-111.7,-70.3,10.7895355526966));
#17282=CARTESIAN_POINT('Origin',(-111.7,-70.3,10.4895355526966));
#17283=CARTESIAN_POINT('Origin',(-111.7,-70.3,10.4895355526966));
#17284=CARTESIAN_POINT('Origin',(-62.7242640687119,-89.7,3.08953555269655));
#17285=CARTESIAN_POINT('',(-62.512132034356,-89.7,3.30166758705252));
#17286=CARTESIAN_POINT('Origin',(-62.7242640687119,-89.7,3.08953555269655));
#17287=CARTESIAN_POINT('',(-62.7242640687119,-90.,3.08953555269655));
#17288=CARTESIAN_POINT('Origin',(-62.7242640687119,-89.7,3.08953555269655));
#17289=CARTESIAN_POINT('Origin',(-62.7242640687119,-89.7,3.08953555269655));
#17290=CARTESIAN_POINT('Origin',(-70.1242640687119,-70.3,10.4895355526966));
#17291=CARTESIAN_POINT('',(-70.1242640687119,-70.3,10.7895355526966));
#17292=CARTESIAN_POINT('',(-70.1242640687119,-70.,10.4895355526966));
#17293=CARTESIAN_POINT('Origin',(-70.1242640687119,-70.3,10.4895355526966));
#17294=CARTESIAN_POINT('',(-69.9121320343559,-70.3,10.7016675870525));
#17295=CARTESIAN_POINT('Origin',(-70.1242640687119,-70.3,10.4895355526966));
#17296=CARTESIAN_POINT('Origin',(-70.1242640687119,-70.3,10.4895355526966));
#17297=CARTESIAN_POINT('Origin',(-111.7,-89.7,10.4895355526966));
#17298=CARTESIAN_POINT('',(-112.,-89.7,10.4895355526966));
#17299=CARTESIAN_POINT('',(-111.7,-89.7,10.7895355526966));
#17300=CARTESIAN_POINT('Origin',(-111.7,-89.7,10.4895355526966));
#17301=CARTESIAN_POINT('',(-111.7,-90.,10.4895355526966));
#17302=CARTESIAN_POINT('Origin',(-111.7,-89.7,10.4895355526966));
#17303=CARTESIAN_POINT('Origin',(-111.7,-89.7,10.4895355526966));
#17304=CARTESIAN_POINT('Origin',(-111.7,-89.7,2.69738388817414));
#17305=CARTESIAN_POINT('',(-112.,-89.7,2.69738388817414));
#17306=CARTESIAN_POINT('',(-111.7,-90.,2.69738388817414));
#17307=CARTESIAN_POINT('Origin',(-70.1242640687119,-89.7,10.4895355526966));
#17308=CARTESIAN_POINT('',(-70.1242640687119,-89.7,10.7895355526966));
#17309=CARTESIAN_POINT('',(-69.9121320343559,-89.7,10.7016675870525));
#17310=CARTESIAN_POINT('Origin',(-70.1242640687119,-89.7,10.4895355526966));
#17311=CARTESIAN_POINT('',(-70.1242640687119,-90.,10.4895355526966));
#17312=CARTESIAN_POINT('Origin',(-70.1242640687119,-89.7,10.4895355526966));
#17313=CARTESIAN_POINT('Origin',(-70.1242640687119,-89.7,10.4895355526966));
#17314=CARTESIAN_POINT('Origin',(-99.5,-89.7,10.4895355526966));
#17315=CARTESIAN_POINT('',(-99.5,-90.,10.4895355526966));
#17316=CARTESIAN_POINT('',(-99.5,-89.7,10.7895355526966));
#17317=CARTESIAN_POINT('Origin',(-73.1134400902689,-89.7,13.4787115742535));
#17318=CARTESIAN_POINT('',(-73.1134400902689,-90.,13.4787115742535));
#17319=CARTESIAN_POINT('',(-72.9013080559129,-89.7,13.6908436086095));
#17320=CARTESIAN_POINT('Origin',(-70.1242640687119,-90.,10.4895355526966));
#17321=CARTESIAN_POINT('',(-70.1242640687119,-90.,10.7895355526966));
#17322=CARTESIAN_POINT('',(-69.9121320343559,-90.,10.7016675870525));
#17323=CARTESIAN_POINT('Origin',(-111.7,-90.,10.4895355526966));
#17324=CARTESIAN_POINT('',(-112.,-90.,10.4895355526966));
#17325=CARTESIAN_POINT('',(-111.7,-90.,10.7895355526966));
#17326=CARTESIAN_POINT('Origin',(-73.1134400902689,-70.3,13.4787115742535));
#17327=CARTESIAN_POINT('',(-73.1134400902689,-70.,13.4787115742535));
#17328=CARTESIAN_POINT('',(-72.9013080559129,-70.3,13.6908436086095));
#17329=CARTESIAN_POINT('Origin',(-99.5,-70.3,10.4895355526966));
#17330=CARTESIAN_POINT('',(-99.5,-70.,10.4895355526966));
#17331=CARTESIAN_POINT('',(-99.5,-70.3,10.7895355526966));
#17332=CARTESIAN_POINT('Origin',(-74.5,-89.7,3.08953555269655));
#17333=CARTESIAN_POINT('',(-74.5,-90.,3.08953555269655));
#17334=CARTESIAN_POINT('Origin',(-62.7242640687119,-90.,3.08953555269655));
#17335=CARTESIAN_POINT('',(-62.512132034356,-90.,3.30166758705252));
#17336=CARTESIAN_POINT('Origin',(-111.7,-70.3,2.69738388817414));
#17337=CARTESIAN_POINT('',(-111.7,-70.,2.69738388817414));
#17338=CARTESIAN_POINT('',(-112.,-70.3,2.69738388817414));
#17339=CARTESIAN_POINT('Origin',(-111.7,-90.,0.3));
#17340=CARTESIAN_POINT('',(-111.7,-90.,0.));
#17341=CARTESIAN_POINT('',(-112.,-90.,0.3));
#17342=CARTESIAN_POINT('Origin',(-74.5,-70.3,3.08953555269655));
#17343=CARTESIAN_POINT('',(-74.5,-70.,3.08953555269655));
#17344=CARTESIAN_POINT('Origin',(-109.7,-90.,2.48953555269655));
#17345=CARTESIAN_POINT('',(-110.,-90.,2.48953555269655));
#17346=CARTESIAN_POINT('Origin',(-98.5,-70.3,0.3));
#17347=CARTESIAN_POINT('',(-110.,-70.3,0.));
#17348=CARTESIAN_POINT('',(-98.5,-70.3,0.));
#17349=CARTESIAN_POINT('',(-110.3,-70.,0.3));
#17350=CARTESIAN_POINT('',(-98.5,-70.,0.3));
#17351=CARTESIAN_POINT('Origin',(-110.3,-70.3,0.3));
#17352=CARTESIAN_POINT('Origin',(-110.3,-70.3,4.09215166452241));
#17353=CARTESIAN_POINT('',(-110.3,-70.,4.09215166452241));
#17354=CARTESIAN_POINT('',(-110.,-70.3,4.09215166452241));
#17355=CARTESIAN_POINT('Origin',(-110.,-90.,2.78953555269655));
#17356=CARTESIAN_POINT('',(-110.,-90.,0.));
#17357=CARTESIAN_POINT('Origin',(-87.,-90.,5.39476777634828));
#17358=CARTESIAN_POINT('Origin',(-112.,-90.,0.));
#17359=CARTESIAN_POINT('Origin',(-112.,-90.,10.7895355526966));
#17360=CARTESIAN_POINT('',(-104.475451921837,-84.8,10.7895355526966));
#17361=CARTESIAN_POINT('',(-77.8080528673835,-84.8,10.7895355526966));
#17362=CARTESIAN_POINT('',(-94.9040264336917,-84.8,10.7895355526966));
#17363=CARTESIAN_POINT('',(-104.475451921837,-75.2,10.7895355526966));
#17364=CARTESIAN_POINT('Origin',(-104.475451921837,-80.,10.7895355526966));
#17365=CARTESIAN_POINT('',(-77.8080528673835,-75.2,10.7895355526966));
#17366=CARTESIAN_POINT('',(-108.237725960918,-75.2,10.7895355526966));
#17367=CARTESIAN_POINT('Origin',(-77.8080528673835,-80.,10.7895355526966));
#17368=CARTESIAN_POINT('Origin',(-70.,-90.,10.7895355526965));
#17369=CARTESIAN_POINT('Origin',(-87.,-70.,5.39476777634828));
#17370=CARTESIAN_POINT('Origin',(-94.9040264336917,-84.8,10.4895355526966));
#17371=CARTESIAN_POINT('Origin',(-77.8080528673835,-84.8,10.4895355526966));
#17372=CARTESIAN_POINT('Origin',(-104.475451921837,-84.8,10.4895355526966));
#17373=CARTESIAN_POINT('Origin',(-104.475451921837,-80.,10.4895355526966));
#17374=CARTESIAN_POINT('',(-104.475451921837,-75.5,10.4895355526966));
#17375=CARTESIAN_POINT('Origin',(-104.475451921837,-75.2,10.4895355526966));
#17376=CARTESIAN_POINT('Origin',(-104.475451921837,-80.,10.4895355526966));
#17377=CARTESIAN_POINT('Origin',(-108.237725960918,-75.2,10.4895355526966));
#17378=CARTESIAN_POINT('Origin',(-77.8080528673835,-75.2,10.4895355526966));
#17379=CARTESIAN_POINT('',(-108.237725960918,-75.5,10.4895355526966));
#17380=CARTESIAN_POINT('Origin',(-77.8080528673835,-80.,10.4895355526966));
#17381=CARTESIAN_POINT('Origin',(-104.475451921837,-80.,10.7895355526966));
#17382=CARTESIAN_POINT('',(-104.475451921837,-75.5,10.7895355526966));
#17383=CARTESIAN_POINT('Origin',(-104.475451921837,-75.5,10.7895355526966));
#17384=CARTESIAN_POINT('Origin',(-110.,-90.,0.));
#17820=UNCERTAINTY_MEASURE_WITH_UNIT(LENGTH_MEASURE(0.01),#17837,
'DISTANCE_ACCURACY_VALUE',
'Maximum model space distance between geometric entities at asserted c
onnectivities');
#17824=UNCERTAINTY_MEASURE_WITH_UNIT(LENGTH_MEASURE(0.01),#17837,
'DISTANCE_ACCURACY_VALUE',
'Maximum model space distance between geometric entities at asserted c
onnectivities');
#17832=(
GEOMETRIC_REPRESENTATION_CONTEXT(3)
GLOBAL_UNCERTAINTY_ASSIGNED_CONTEXT((#17820))
GLOBAL_UNIT_ASSIGNED_CONTEXT((#17837,#17839,#17840))
REPRESENTATION_CONTEXT('','3D')
);
#17836=(
GEOMETRIC_REPRESENTATION_CONTEXT(3)
GLOBAL_UNCERTAINTY_ASSIGNED_CONTEXT((#17824))
GLOBAL_UNIT_ASSIGNED_CONTEXT((#17837,#17839,#17840))
REPRESENTATION_CONTEXT('','3D')
);
#17837=(
LENGTH_UNIT()
NAMED_UNIT(*)
SI_UNIT(.MILLI.,.METRE.)
);
#17839=(
NAMED_UNIT(*)
PLANE_ANGLE_UNIT()
SI_UNIT($,.RADIAN.)
);
#17840=(
NAMED_UNIT(*)
SI_UNIT($,.STERADIAN.)
SOLID_ANGLE_UNIT()
);
#17848=SHAPE_DEFINITION_REPRESENTATION(#17859,#17880);
#17859=PRODUCT_DEFINITION_SHAPE('',$,#17892);
#17880=SHAPE_REPRESENTATION('',(#10714),#17832);
#17884=PRODUCT_DEFINITION_CONTEXT('part definition',#17919,'design');
#17892=PRODUCT_DEFINITION('Clamp_01','Clamp_01',#17903,#17884);
#17903=PRODUCT_DEFINITION_FORMATION('',$,#17928);
#17919=APPLICATION_CONTEXT(
'Core Data for Automotive Mechanical Design Process');
#17920=PRODUCT_CONTEXT('part definition',#17919,'mechanical');
#17928=PRODUCT('Clamp_01','Clamp_01',$,(#17920));
#17953=COLOUR_RGB('Light Blue',0.38,0.62,0.78);
#17954=FILL_AREA_STYLE_COLOUR('',#17953);
#17955=FILL_AREA_STYLE('',(#17954));
#17956=SURFACE_STYLE_FILL_AREA(#17955);
#17957=SURFACE_SIDE_STYLE('',(#17956));
#17958=SURFACE_STYLE_USAGE(.BOTH.,#17957);
#17959=PRESENTATION_STYLE_ASSIGNMENT((#17958));
ENDSEC;
END-ISO-10303-21;
